ISO-10303-21;
HEADER;
/* Generated by software containing ST-Developer
 * from STEP Tools, Inc. (www.steptools.com) 
 */

FILE_DESCRIPTION(
/* description */ ('Flange-mounted spindle'),
/* implementation_level */ '2;1');

FILE_NAME(
/* name */ 'Cap Screw - M5x20.step',
/* time_stamp */ '2026-10-27T10:49:51-07:00',
/* author */ (''),
/* organization */ (''),
/* preprocessor_version */ 'ST-DEVELOPER v20.2',
/* originating_system */ 'Autodesk Translation Framework v15.17.0.0',
/* authorisation */ '');

FILE_SCHEMA (('AUTOMOTIVE_DESIGN { 1 0 10303 214 3 1 1 }'));
ENDSEC;

DATA;
#10=MECHANICAL_DESIGN_GEOMETRIC_PRESENTATION_REPRESENTATION('',(#361),#11764);
#270=CONICAL_SURFACE('',#7087,0.4,0.785398163397448);
#271=CONICAL_SURFACE('',#7091,0.41,0.785398163397448);
#272=CONICAL_SURFACE('',#7095,0.26,0.463647609000806);
#273=CONICAL_SURFACE('',#7099,0.225,0.785398163397448);
#280=ORIENTED_CLOSED_SHELL('',*,#6156,.F.);
#283=BREP_WITH_VOIDS('Body1',#6155,(#280));
#306=SHAPE_REPRESENTATION_RELATIONSHIP('SRR','None',#11904,#333);
#333=ADVANCED_BREP_SHAPE_REPRESENTATION('',(#283),#11759);
#361=STYLED_ITEM('',(#12106),#283);
#500=FACE_BOUND('',#1424,.T.);
#634=PLANE('',#7085);
#635=PLANE('',#7093);
#636=PLANE('',#7101);
#637=PLANE('',#7102);
#638=PLANE('',#7103);
#639=PLANE('',#7104);
#640=PLANE('',#7105);
#641=PLANE('',#7106);
#642=PLANE('',#7107);
#643=PLANE('',#7108);
#644=PLANE('',#7109);
#965=FACE_OUTER_BOUND('',#1419,.T.);
#966=FACE_OUTER_BOUND('',#1420,.T.);
#967=FACE_OUTER_BOUND('',#1421,.T.);
#968=FACE_OUTER_BOUND('',#1422,.T.);
#969=FACE_OUTER_BOUND('',#1423,.T.);
#970=FACE_OUTER_BOUND('',#1425,.T.);
#971=FACE_OUTER_BOUND('',#1426,.T.);
#972=FACE_OUTER_BOUND('',#1427,.T.);
#973=FACE_OUTER_BOUND('',#1428,.T.);
#974=FACE_OUTER_BOUND('',#1429,.T.);
#975=FACE_OUTER_BOUND('',#1430,.T.);
#976=FACE_OUTER_BOUND('',#1431,.T.);
#977=FACE_OUTER_BOUND('',#1432,.T.);
#978=FACE_OUTER_BOUND('',#1433,.T.);
#979=FACE_OUTER_BOUND('',#1434,.T.);
#980=FACE_OUTER_BOUND('',#1435,.T.);
#981=FACE_OUTER_BOUND('',#1436,.T.);
#1419=EDGE_LOOP('',(#5401));
#1420=EDGE_LOOP('',(#5402,#5403,#5404,#5405));
#1421=EDGE_LOOP('',(#5406,#5407,#5408,#5409));
#1422=EDGE_LOOP('',(#5410,#5411,#5412,#5413));
#1423=EDGE_LOOP('',(#5414));
#1424=EDGE_LOOP('',(#5415));
#1425=EDGE_LOOP('',(#5416,#5417,#5418,#5419));
#1426=EDGE_LOOP('',(#5420,#5421,#5422,#5423));
#1427=EDGE_LOOP('',(#5424,#5425,#5426,#5427));
#1428=EDGE_LOOP('',(#5428));
#1429=EDGE_LOOP('',(#5429,#5430,#5431,#5432));
#1430=EDGE_LOOP('',(#5433,#5434,#5435,#5436));
#1431=EDGE_LOOP('',(#5437,#5438,#5439,#5440));
#1432=EDGE_LOOP('',(#5441,#5442,#5443,#5444));
#1433=EDGE_LOOP('',(#5445,#5446,#5447,#5448));
#1434=EDGE_LOOP('',(#5449,#5450,#5451,#5452));
#1435=EDGE_LOOP('',(#5453,#5454,#5455,#5456,#5457,#5458));
#1436=EDGE_LOOP('',(#5459,#5460,#5461,#5462,#5463,#5464));
#1821=LINE('',#11396,#2243);
#1822=LINE('',#11400,#2244);
#1823=LINE('',#11404,#2245);
#1824=LINE('',#11411,#2246);
#1825=LINE('',#11415,#2247);
#1826=LINE('',#11419,#2248);
#1827=LINE('',#11424,#2249);
#1828=LINE('',#11426,#2250);
#1829=LINE('',#11428,#2251);
#1830=LINE('',#11429,#2252);
#1831=LINE('',#11432,#2253);
#1832=LINE('',#11434,#2254);
#1833=LINE('',#11435,#2255);
#1834=LINE('',#11438,#2256);
#1835=LINE('',#11440,#2257);
#1836=LINE('',#11441,#2258);
#1837=LINE('',#11444,#2259);
#1838=LINE('',#11446,#2260);
#1839=LINE('',#11447,#2261);
#1840=LINE('',#11450,#2262);
#1841=LINE('',#11452,#2263);
#1842=LINE('',#11453,#2264);
#1843=LINE('',#11455,#2265);
#1844=LINE('',#11456,#2266);
#2243=VECTOR('',#8810,0.4);
#2244=VECTOR('',#8815,0.425);
#2245=VECTOR('',#8820,0.41);
#2246=VECTOR('',#8829,0.26);
#2247=VECTOR('',#8834,0.25);
#2248=VECTOR('',#8839,0.225);
#2249=VECTOR('',#8844,1.);
#2250=VECTOR('',#8845,1.);
#2251=VECTOR('',#8846,1.);
#2252=VECTOR('',#8847,1.);
#2253=VECTOR('',#8850,1.);
#2254=VECTOR('',#8851,1.);
#2255=VECTOR('',#8852,1.);
#2256=VECTOR('',#8855,1.);
#2257=VECTOR('',#8856,1.);
#2258=VECTOR('',#8857,1.);
#2259=VECTOR('',#8860,1.);
#2260=VECTOR('',#8861,1.);
#2261=VECTOR('',#8862,1.);
#2262=VECTOR('',#8865,1.);
#2263=VECTOR('',#8866,1.);
#2264=VECTOR('',#8867,1.);
#2265=VECTOR('',#8870,1.);
#2266=VECTOR('',#8871,1.);
#2629=CIRCLE('',#7086,0.375);
#2630=CIRCLE('',#7088,0.425);
#2631=CIRCLE('',#7090,0.425);
#2632=CIRCLE('',#7092,0.395);
#2633=CIRCLE('',#7094,0.27);
#2634=CIRCLE('',#7096,0.24505);
#2635=CIRCLE('',#7098,0.24505);
#2636=CIRCLE('',#7100,0.2);
#3123=VERTEX_POINT('',#11391);
#3124=VERTEX_POINT('',#11394);
#3125=VERTEX_POINT('',#11398);
#3126=VERTEX_POINT('',#11402);
#3127=VERTEX_POINT('',#11406);
#3128=VERTEX_POINT('',#11409);
#3129=VERTEX_POINT('',#11413);
#3130=VERTEX_POINT('',#11417);
#3131=VERTEX_POINT('',#11422);
#3132=VERTEX_POINT('',#11423);
#3133=VERTEX_POINT('',#11425);
#3134=VERTEX_POINT('',#11427);
#3135=VERTEX_POINT('',#11431);
#3136=VERTEX_POINT('',#11433);
#3137=VERTEX_POINT('',#11437);
#3138=VERTEX_POINT('',#11439);
#3139=VERTEX_POINT('',#11443);
#3140=VERTEX_POINT('',#11445);
#3141=VERTEX_POINT('',#11449);
#3142=VERTEX_POINT('',#11451);
#3893=EDGE_CURVE('',#3123,#3123,#2629,.T.);
#3894=EDGE_CURVE('',#3124,#3124,#2630,.T.);
#3895=EDGE_CURVE('',#3124,#3123,#1821,.T.);
#3896=EDGE_CURVE('',#3125,#3125,#2631,.T.);
#3897=EDGE_CURVE('',#3125,#3124,#1822,.T.);
#3898=EDGE_CURVE('',#3126,#3126,#2632,.T.);
#3899=EDGE_CURVE('',#3126,#3125,#1823,.T.);
#3900=EDGE_CURVE('',#3127,#3127,#2633,.T.);
#3901=EDGE_CURVE('',#3128,#3128,#2634,.F.);
#3902=EDGE_CURVE('',#3128,#3127,#1824,.T.);
#3903=EDGE_CURVE('',#3129,#3129,#2635,.F.);
#3904=EDGE_CURVE('',#3129,#3128,#1825,.T.);
#3905=EDGE_CURVE('',#3130,#3130,#2636,.T.);
#3906=EDGE_CURVE('',#3130,#3129,#1826,.T.);
#3907=EDGE_CURVE('',#3131,#3132,#1827,.T.);
#3908=EDGE_CURVE('',#3132,#3133,#1828,.T.);
#3909=EDGE_CURVE('',#3133,#3134,#1829,.T.);
#3910=EDGE_CURVE('',#3131,#3134,#1830,.T.);
#3911=EDGE_CURVE('',#3132,#3135,#1831,.T.);
#3912=EDGE_CURVE('',#3135,#3136,#1832,.T.);
#3913=EDGE_CURVE('',#3136,#3133,#1833,.T.);
#3914=EDGE_CURVE('',#3135,#3137,#1834,.T.);
#3915=EDGE_CURVE('',#3137,#3138,#1835,.T.);
#3916=EDGE_CURVE('',#3138,#3136,#1836,.T.);
#3917=EDGE_CURVE('',#3137,#3139,#1837,.T.);
#3918=EDGE_CURVE('',#3139,#3140,#1838,.T.);
#3919=EDGE_CURVE('',#3140,#3138,#1839,.T.);
#3920=EDGE_CURVE('',#3139,#3141,#1840,.T.);
#3921=EDGE_CURVE('',#3141,#3142,#1841,.T.);
#3922=EDGE_CURVE('',#3142,#3140,#1842,.T.);
#3923=EDGE_CURVE('',#3141,#3131,#1843,.T.);
#3924=EDGE_CURVE('',#3134,#3142,#1844,.T.);
#5401=ORIENTED_EDGE('',*,*,#3893,.F.);
#5402=ORIENTED_EDGE('',*,*,#3894,.F.);
#5403=ORIENTED_EDGE('',*,*,#3895,.T.);
#5404=ORIENTED_EDGE('',*,*,#3893,.T.);
#5405=ORIENTED_EDGE('',*,*,#3895,.F.);
#5406=ORIENTED_EDGE('',*,*,#3896,.F.);
#5407=ORIENTED_EDGE('',*,*,#3897,.T.);
#5408=ORIENTED_EDGE('',*,*,#3894,.T.);
#5409=ORIENTED_EDGE('',*,*,#3897,.F.);
#5410=ORIENTED_EDGE('',*,*,#3898,.F.);
#5411=ORIENTED_EDGE('',*,*,#3899,.T.);
#5412=ORIENTED_EDGE('',*,*,#3896,.T.);
#5413=ORIENTED_EDGE('',*,*,#3899,.F.);
#5414=ORIENTED_EDGE('',*,*,#3898,.T.);
#5415=ORIENTED_EDGE('',*,*,#3900,.F.);
#5416=ORIENTED_EDGE('',*,*,#3901,.F.);
#5417=ORIENTED_EDGE('',*,*,#3902,.T.);
#5418=ORIENTED_EDGE('',*,*,#3900,.T.);
#5419=ORIENTED_EDGE('',*,*,#3902,.F.);
#5420=ORIENTED_EDGE('',*,*,#3903,.F.);
#5421=ORIENTED_EDGE('',*,*,#3904,.T.);
#5422=ORIENTED_EDGE('',*,*,#3901,.T.);
#5423=ORIENTED_EDGE('',*,*,#3904,.F.);
#5424=ORIENTED_EDGE('',*,*,#3905,.F.);
#5425=ORIENTED_EDGE('',*,*,#3906,.T.);
#5426=ORIENTED_EDGE('',*,*,#3903,.T.);
#5427=ORIENTED_EDGE('',*,*,#3906,.F.);
#5428=ORIENTED_EDGE('',*,*,#3905,.T.);
#5429=ORIENTED_EDGE('',*,*,#3907,.T.);
#5430=ORIENTED_EDGE('',*,*,#3908,.T.);
#5431=ORIENTED_EDGE('',*,*,#3909,.T.);
#5432=ORIENTED_EDGE('',*,*,#3910,.F.);
#5433=ORIENTED_EDGE('',*,*,#3911,.T.);
#5434=ORIENTED_EDGE('',*,*,#3912,.T.);
#5435=ORIENTED_EDGE('',*,*,#3913,.T.);
#5436=ORIENTED_EDGE('',*,*,#3908,.F.);
#5437=ORIENTED_EDGE('',*,*,#3914,.T.);
#5438=ORIENTED_EDGE('',*,*,#3915,.T.);
#5439=ORIENTED_EDGE('',*,*,#3916,.T.);
#5440=ORIENTED_EDGE('',*,*,#3912,.F.);
#5441=ORIENTED_EDGE('',*,*,#3917,.T.);
#5442=ORIENTED_EDGE('',*,*,#3918,.T.);
#5443=ORIENTED_EDGE('',*,*,#3919,.T.);
#5444=ORIENTED_EDGE('',*,*,#3915,.F.);
#5445=ORIENTED_EDGE('',*,*,#3920,.T.);
#5446=ORIENTED_EDGE('',*,*,#3921,.T.);
#5447=ORIENTED_EDGE('',*,*,#3922,.T.);
#5448=ORIENTED_EDGE('',*,*,#3918,.F.);
#5449=ORIENTED_EDGE('',*,*,#3923,.T.);
#5450=ORIENTED_EDGE('',*,*,#3910,.T.);
#5451=ORIENTED_EDGE('',*,*,#3924,.T.);
#5452=ORIENTED_EDGE('',*,*,#3921,.F.);
#5453=ORIENTED_EDGE('',*,*,#3923,.F.);
#5454=ORIENTED_EDGE('',*,*,#3920,.F.);
#5455=ORIENTED_EDGE('',*,*,#3917,.F.);
#5456=ORIENTED_EDGE('',*,*,#3914,.F.);
#5457=ORIENTED_EDGE('',*,*,#3911,.F.);
#5458=ORIENTED_EDGE('',*,*,#3907,.F.);
#5459=ORIENTED_EDGE('',*,*,#3924,.F.);
#5460=ORIENTED_EDGE('',*,*,#3909,.F.);
#5461=ORIENTED_EDGE('',*,*,#3913,.F.);
#5462=ORIENTED_EDGE('',*,*,#3916,.F.);
#5463=ORIENTED_EDGE('',*,*,#3919,.F.);
#5464=ORIENTED_EDGE('',*,*,#3922,.F.);
#5779=CYLINDRICAL_SURFACE('',#7089,0.425);
#5780=CYLINDRICAL_SURFACE('',#7097,0.24505);
#6076=ADVANCED_FACE('',(#965),#634,.T.);
#6077=ADVANCED_FACE('',(#966),#270,.T.);
#6078=ADVANCED_FACE('',(#967),#5779,.T.);
#6079=ADVANCED_FACE('',(#968),#271,.T.);
#6080=ADVANCED_FACE('',(#969,#500),#635,.T.);
#6081=ADVANCED_FACE('',(#970),#272,.T.);
#6082=ADVANCED_FACE('',(#971),#5780,.T.);
#6083=ADVANCED_FACE('',(#972),#273,.T.);
#6084=ADVANCED_FACE('',(#973),#636,.T.);
#6085=ADVANCED_FACE('',(#974),#637,.F.);
#6086=ADVANCED_FACE('',(#975),#638,.F.);
#6087=ADVANCED_FACE('',(#976),#639,.F.);
#6088=ADVANCED_FACE('',(#977),#640,.F.);
#6089=ADVANCED_FACE('',(#978),#641,.F.);
#6090=ADVANCED_FACE('',(#979),#642,.F.);
#6091=ADVANCED_FACE('',(#980),#643,.F.);
#6092=ADVANCED_FACE('',(#981),#644,.F.);
#6155=CLOSED_SHELL('',(#6076,#6077,#6078,#6079,#6080,#6081,#6082,#6083,
#6084));
#6156=CLOSED_SHELL('',(#6085,#6086,#6087,#6088,#6089,#6090,#6091,#6092));
#7084=AXIS2_PLACEMENT_3D('',#11389,#8800,#8801);
#7085=AXIS2_PLACEMENT_3D('',#11390,#8802,#8803);
#7086=AXIS2_PLACEMENT_3D('',#11392,#8804,#8805);
#7087=AXIS2_PLACEMENT_3D('',#11393,#8806,#8807);
#7088=AXIS2_PLACEMENT_3D('',#11395,#8808,#8809);
#7089=AXIS2_PLACEMENT_3D('',#11397,#8811,#8812);
#7090=AXIS2_PLACEMENT_3D('',#11399,#8813,#8814);
#7091=AXIS2_PLACEMENT_3D('',#11401,#8816,#8817);
#7092=AXIS2_PLACEMENT_3D('',#11403,#8818,#8819);
#7093=AXIS2_PLACEMENT_3D('',#11405,#8821,#8822);
#7094=AXIS2_PLACEMENT_3D('',#11407,#8823,#8824);
#7095=AXIS2_PLACEMENT_3D('',#11408,#8825,#8826);
#7096=AXIS2_PLACEMENT_3D('',#11410,#8827,#8828);
#7097=AXIS2_PLACEMENT_3D('',#11412,#8830,#8831);
#7098=AXIS2_PLACEMENT_3D('',#11414,#8832,#8833);
#7099=AXIS2_PLACEMENT_3D('',#11416,#8835,#8836);
#7100=AXIS2_PLACEMENT_3D('',#11418,#8837,#8838);
#7101=AXIS2_PLACEMENT_3D('',#11420,#8840,#8841);
#7102=AXIS2_PLACEMENT_3D('',#11421,#8842,#8843);
#7103=AXIS2_PLACEMENT_3D('',#11430,#8848,#8849);
#7104=AXIS2_PLACEMENT_3D('',#11436,#8853,#8854);
#7105=AXIS2_PLACEMENT_3D('',#11442,#8858,#8859);
#7106=AXIS2_PLACEMENT_3D('',#11448,#8863,#8864);
#7107=AXIS2_PLACEMENT_3D('',#11454,#8868,#8869);
#7108=AXIS2_PLACEMENT_3D('',#11457,#8872,#8873);
#7109=AXIS2_PLACEMENT_3D('',#11458,#8874,#8875);
#8800=DIRECTION('axis',(0.,0.,1.));
#8801=DIRECTION('refdir',(1.,0.,0.));
#8802=DIRECTION('center_axis',(0.,1.,0.));
#8803=DIRECTION('ref_axis',(0.,0.,1.));
#8804=DIRECTION('center_axis',(0.,-1.,0.));
#8805=DIRECTION('ref_axis',(1.,0.,0.));
#8806=DIRECTION('center_axis',(0.,-1.,0.));
#8807=DIRECTION('ref_axis',(1.,0.,0.));
#8808=DIRECTION('center_axis',(0.,-1.,0.));
#8809=DIRECTION('ref_axis',(1.,0.,0.));
#8810=DIRECTION('',(0.707106781186548,0.707106781186547,8.65956056235493E-17));
#8811=DIRECTION('center_axis',(0.,-1.,0.));
#8812=DIRECTION('ref_axis',(1.,0.,0.));
#8813=DIRECTION('center_axis',(0.,-1.,0.));
#8814=DIRECTION('ref_axis',(1.,0.,0.));
#8815=DIRECTION('',(0.,1.,0.));
#8816=DIRECTION('center_axis',(0.,1.,0.));
#8817=DIRECTION('ref_axis',(1.,0.,0.));
#8818=DIRECTION('center_axis',(0.,-1.,0.));
#8819=DIRECTION('ref_axis',(1.,0.,0.));
#8820=DIRECTION('',(-0.707106781186547,0.707106781186548,-8.65956056235493E-17));
#8821=DIRECTION('center_axis',(0.,-1.,0.));
#8822=DIRECTION('ref_axis',(0.,0.,-1.));
#8823=DIRECTION('center_axis',(0.,-1.,0.));
#8824=DIRECTION('ref_axis',(1.,0.,0.));
#8825=DIRECTION('center_axis',(0.,1.,0.));
#8826=DIRECTION('ref_axis',(1.,0.,0.));
#8827=DIRECTION('center_axis',(0.,1.,0.));
#8828=DIRECTION('ref_axis',(1.,0.,0.));
#8829=DIRECTION('',(-0.447213595499958,0.894427190999916,-5.47678698264203E-17));
#8830=DIRECTION('center_axis',(0.,-1.,0.));
#8831=DIRECTION('ref_axis',(1.,0.,0.));
#8832=DIRECTION('center_axis',(0.,1.,0.));
#8833=DIRECTION('ref_axis',(1.,0.,0.));
#8834=DIRECTION('',(0.,1.,0.));
#8835=DIRECTION('center_axis',(0.,1.,0.));
#8836=DIRECTION('ref_axis',(1.,0.,0.));
#8837=DIRECTION('center_axis',(0.,-1.,0.));
#8838=DIRECTION('ref_axis',(1.,0.,0.));
#8839=DIRECTION('',(-0.707106781186547,0.707106781186548,-8.65956056235493E-17));
#8840=DIRECTION('center_axis',(0.,-1.,0.));
#8841=DIRECTION('ref_axis',(0.,0.,-1.));
#8842=DIRECTION('center_axis',(0.866025403784439,0.,-0.5));
#8843=DIRECTION('ref_axis',(0.5,0.,0.866025403784439));
#8844=DIRECTION('',(-0.5,0.,-0.866025403784439));
#8845=DIRECTION('',(0.,-1.,0.));
#8846=DIRECTION('',(0.5,0.,0.866025403784439));
#8847=DIRECTION('',(0.,-1.,0.));
#8848=DIRECTION('center_axis',(1.20185167898973E-16,0.,-1.));
#8849=DIRECTION('ref_axis',(1.,0.,1.20185167898973E-16));
#8850=DIRECTION('',(-1.,0.,-1.20185167898973E-16));
#8851=DIRECTION('',(0.,-1.,0.));
#8852=DIRECTION('',(1.,0.,1.20185167898973E-16));
#8853=DIRECTION('center_axis',(-0.866025403784439,0.,-0.5));
#8854=DIRECTION('ref_axis',(0.5,0.,-0.866025403784439));
#8855=DIRECTION('',(-0.5,0.,0.866025403784439));
#8856=DIRECTION('',(0.,-1.,0.));
#8857=DIRECTION('',(0.5,0.,-0.866025403784439));
#8858=DIRECTION('center_axis',(-0.866025403784439,0.,0.5));
#8859=DIRECTION('ref_axis',(-0.5,0.,-0.866025403784439));
#8860=DIRECTION('',(0.5,0.,0.866025403784439));
#8861=DIRECTION('',(0.,-1.,0.));
#8862=DIRECTION('',(-0.5,0.,-0.866025403784439));
#8863=DIRECTION('center_axis',(-2.40370335797945E-16,0.,1.));
#8864=DIRECTION('ref_axis',(-1.,0.,-2.40370335797945E-16));
#8865=DIRECTION('',(1.,0.,2.40370335797945E-16));
#8866=DIRECTION('',(0.,-1.,0.));
#8867=DIRECTION('',(-1.,0.,-2.40370335797945E-16));
#8868=DIRECTION('center_axis',(0.866025403784439,0.,0.5));
#8869=DIRECTION('ref_axis',(-0.5,0.,0.866025403784439));
#8870=DIRECTION('',(0.5,0.,-0.866025403784439));
#8871=DIRECTION('',(-0.5,0.,0.866025403784439));
#8872=DIRECTION('center_axis',(0.,1.,0.));
#8873=DIRECTION('ref_axis',(1.,0.,0.));
#8874=DIRECTION('center_axis',(0.,-1.,0.));
#8875=DIRECTION('ref_axis',(0.,0.,-1.));
#11389=CARTESIAN_POINT('',(0.,0.,0.));
#11390=CARTESIAN_POINT('Origin',(0.375,0.5,0.));
#11391=CARTESIAN_POINT('',(-0.375,0.5,-4.59242549680257E-17));
#11392=CARTESIAN_POINT('Origin',(0.,0.5,0.));
#11393=CARTESIAN_POINT('Origin',(0.,0.475,0.));
#11394=CARTESIAN_POINT('',(-0.425,0.45,-5.20474889637625E-17));
#11395=CARTESIAN_POINT('Origin',(0.,0.45,0.));
#11396=CARTESIAN_POINT('',(-0.4,0.475,-4.89858719658941E-17));
#11397=CARTESIAN_POINT('Origin',(0.,0.24,0.));
#11398=CARTESIAN_POINT('',(-0.425,0.0299999999999998,-5.20474889637625E-17));
#11399=CARTESIAN_POINT('Origin',(0.,0.0299999999999998,0.));
#11400=CARTESIAN_POINT('',(-0.425,0.24,-5.20474889637625E-17));
#11401=CARTESIAN_POINT('Origin',(0.,0.0150000000000001,0.));
#11402=CARTESIAN_POINT('',(-0.395,4.85722573273506E-17,-4.83735485663204E-17));
#11403=CARTESIAN_POINT('Origin',(0.,0.,0.));
#11404=CARTESIAN_POINT('',(-0.41,0.0150000000000001,-5.02105187650415E-17));
#11405=CARTESIAN_POINT('Origin',(0.27,0.,0.));
#11406=CARTESIAN_POINT('',(-0.27,0.,-3.30654635769785E-17));
#11407=CARTESIAN_POINT('Origin',(0.,0.,0.));
#11408=CARTESIAN_POINT('Origin',(0.,-0.02,0.));
#11409=CARTESIAN_POINT('',(-0.24505,-0.0498999999999999,3.00099698131059E-17));
#11410=CARTESIAN_POINT('Origin',(0.,-0.0498999999999999,0.));
#11411=CARTESIAN_POINT('',(-0.26,-0.02,-3.18408167778312E-17));
#11412=CARTESIAN_POINT('Origin',(0.,-0.995,0.));
#11413=CARTESIAN_POINT('',(-0.24505,-1.95495,3.00099698131059E-17));
#11414=CARTESIAN_POINT('Origin',(0.,-1.95495,0.));
#11415=CARTESIAN_POINT('',(-0.24505,-0.995,-3.00099698131059E-17));
#11416=CARTESIAN_POINT('Origin',(0.,-1.975,0.));
#11417=CARTESIAN_POINT('',(-0.2,-2.,-2.44929359829471E-17));
#11418=CARTESIAN_POINT('Origin',(0.,-2.,0.));
#11419=CARTESIAN_POINT('',(-0.225,-1.975,-2.75545529808154E-17));
#11420=CARTESIAN_POINT('Origin',(0.,-2.,0.));
#11421=CARTESIAN_POINT('Origin',(0.115470053837925,-0.5,-0.2));
#11422=CARTESIAN_POINT('',(0.23094010767585,-0.5,0.));
#11423=CARTESIAN_POINT('',(0.115470053837925,-0.5,-0.2));
#11424=CARTESIAN_POINT('',(0.23094010767585,-0.5,0.));
#11425=CARTESIAN_POINT('',(0.115470053837925,-0.8,-0.2));
#11426=CARTESIAN_POINT('',(0.115470053837925,-0.5,-0.2));
#11427=CARTESIAN_POINT('',(0.23094010767585,-0.8,0.));
#11428=CARTESIAN_POINT('',(0.23094010767585,-0.8,0.));
#11429=CARTESIAN_POINT('',(0.23094010767585,-0.5,0.));
#11430=CARTESIAN_POINT('Origin',(-0.115470053837925,-0.5,-0.2));
#11431=CARTESIAN_POINT('',(-0.115470053837925,-0.5,-0.2));
#11432=CARTESIAN_POINT('',(0.115470053837925,-0.5,-0.2));
#11433=CARTESIAN_POINT('',(-0.115470053837925,-0.8,-0.2));
#11434=CARTESIAN_POINT('',(-0.115470053837925,-0.5,-0.2));
#11435=CARTESIAN_POINT('',(0.115470053837925,-0.8,-0.2));
#11436=CARTESIAN_POINT('Origin',(-0.23094010767585,-0.5,-2.77555756156289E-17));
#11437=CARTESIAN_POINT('',(-0.23094010767585,-0.5,-2.82820063659975E-17));
#11438=CARTESIAN_POINT('',(-0.115470053837925,-0.5,-0.2));
#11439=CARTESIAN_POINT('',(-0.23094010767585,-0.8,-2.77555756156289E-17));
#11440=CARTESIAN_POINT('',(-0.23094010767585,-0.5,-2.82820063659975E-17));
#11441=CARTESIAN_POINT('',(-0.115470053837925,-0.8,-0.2));
#11442=CARTESIAN_POINT('Origin',(-0.115470053837925,-0.5,0.2));
#11443=CARTESIAN_POINT('',(-0.115470053837925,-0.5,0.2));
#11444=CARTESIAN_POINT('',(-0.23094010767585,-0.5,-2.82820063659975E-17));
#11445=CARTESIAN_POINT('',(-0.115470053837925,-0.8,0.2));
#11446=CARTESIAN_POINT('',(-0.115470053837925,-0.5,0.2));
#11447=CARTESIAN_POINT('',(-0.23094010767585,-0.8,-2.82820063659975E-17));
#11448=CARTESIAN_POINT('Origin',(0.115470053837925,-0.5,0.2));
#11449=CARTESIAN_POINT('',(0.115470053837925,-0.5,0.2));
#11450=CARTESIAN_POINT('',(-0.115470053837925,-0.5,0.2));
#11451=CARTESIAN_POINT('',(0.115470053837925,-0.8,0.2));
#11452=CARTESIAN_POINT('',(0.115470053837925,-0.5,0.2));
#11453=CARTESIAN_POINT('',(-0.115470053837925,-0.8,0.2));
#11454=CARTESIAN_POINT('Origin',(0.23094010767585,-0.5,0.));
#11455=CARTESIAN_POINT('',(0.115470053837925,-0.5,0.2));
#11456=CARTESIAN_POINT('',(0.115470053837925,-0.8,0.2));
#11457=CARTESIAN_POINT('Origin',(0.,-0.5,0.));
#11458=CARTESIAN_POINT('Origin',(0.,-0.8,0.));
#11727=UNCERTAINTY_MEASURE_WITH_UNIT(LENGTH_MEASURE(0.001),#11765,
'DISTANCE_ACCURACY_VALUE',
'Maximum model space distance between geometric entities at asserted c
onnectivities');
#11732=UNCERTAINTY_MEASURE_WITH_UNIT(LENGTH_MEASURE(0.001),#11765,
'DISTANCE_ACCURACY_VALUE',
'Maximum model space distance between geometric entities at asserted c
onnectivities');
#11759=(
GEOMETRIC_REPRESENTATION_CONTEXT(3)
GLOBAL_UNCERTAINTY_ASSIGNED_CONTEXT((#11727))
GLOBAL_UNIT_ASSIGNED_CONTEXT((#11765,#11767,#11768))
REPRESENTATION_CONTEXT('','3D')
);
#11764=(
GEOMETRIC_REPRESENTATION_CONTEXT(3)
GLOBAL_UNCERTAINTY_ASSIGNED_CONTEXT((#11732))
GLOBAL_UNIT_ASSIGNED_CONTEXT((#11765,#11767,#11768))
REPRESENTATION_CONTEXT('','3D')
);
#11765=(
LENGTH_UNIT()
NAMED_UNIT(*)
SI_UNIT(.CENTI.,.METRE.)
);
#11767=(
NAMED_UNIT(*)
PLANE_ANGLE_UNIT()
SI_UNIT($,.RADIAN.)
);
#11768=(
NAMED_UNIT(*)
SI_UNIT($,.STERADIAN.)
SOLID_ANGLE_UNIT()
);
#11795=SHAPE_DEFINITION_REPRESENTATION(#11828,#11904);
#11828=PRODUCT_DEFINITION_SHAPE('',$,#11936);
#11904=SHAPE_REPRESENTATION('',(#7084),#11759);
#11909=PRODUCT_DEFINITION_CONTEXT('part definition',#12004,'design');
#11936=PRODUCT_DEFINITION('Cap Screw - M5x20','Cap Screw - M5x20',#11967,
#11909);
#11967=PRODUCT_DEFINITION_FORMATION('',$,#12032);
#12004=APPLICATION_CONTEXT(
'Core Data for Automotive Mechanical Design Process');
#12005=PRODUCT_CONTEXT('part definition',#12004,'mechanical');
#12032=PRODUCT('Cap Screw - M5x20','Cap Screw - M5x20',
'Cap Screw - M5x20',(#12005));
#12100=COLOUR_RGB('Black',0.12,0.14,0.17);
#12101=FILL_AREA_STYLE_COLOUR('',#12100);
#12102=FILL_AREA_STYLE('',(#12101));
#12103=SURFACE_STYLE_FILL_AREA(#12102);
#12104=SURFACE_SIDE_STYLE('',(#12103));
#12105=SURFACE_STYLE_USAGE(.BOTH.,#12104);
#12106=PRESENTATION_STYLE_ASSIGNMENT((#12105));
ENDSEC;
END-ISO-10303-21;
